ISO-10303-21;
HEADER;
/* Generated by software containing ST-Developer
 * from STEP Tools, Inc. (www.steptools.com) 
 */

FILE_DESCRIPTION(
/* description */ ('Independent Peaucellier-Lipkin straight-line linkage. Radius arms 100
 mm, inversion-cell links 60 mm, crank radius and fixed-pivot spacing 
32 mm. Inversion constant 6400 mm squared, nominal output straight lin
e X=100 mm. Overhead bearing bridge clears the layered moving links. N
o accuracy or load rating assigned.'),
/* implementation_level */ '2;1');

FILE_NAME(
/* name */ 'Pivot washer.step',
/* time_stamp */ '2026-11-09T18:06:16-08:00',
/* author */ (''),
/* organization */ (''),
/* preprocessor_version */ 'ST-DEVELOPER v20.2',
/* originating_system */ 'Autodesk Translation Framework v15.17.0.0',
/* authorisation */ '');

FILE_SCHEMA (('AUTOMOTIVE_DESIGN { 1 0 10303 214 3 1 1 }'));
ENDSEC;

DATA;
#10=MECHANICAL_DESIGN_GEOMETRIC_PRESENTATION_REPRESENTATION('',(#297),#3581);
#263=SHAPE_REPRESENTATION_RELATIONSHIP('SRR','None',#3697,#280);
#280=ADVANCED_BREP_SHAPE_REPRESENTATION('',(#314),#3579);
#297=STYLED_ITEM('',(#3786),#314);
#314=MANIFOLD_SOLID_BREP('Body1',#1883);
#362=FACE_BOUND('',#686,.T.);
#363=FACE_BOUND('',#688,.T.);
#419=PLANE('',#2287);
#420=PLANE('',#2288);
#526=FACE_OUTER_BOUND('',#683,.T.);
#527=FACE_OUTER_BOUND('',#684,.T.);
#528=FACE_OUTER_BOUND('',#685,.T.);
#529=FACE_OUTER_BOUND('',#687,.T.);
#683=EDGE_LOOP('',(#1672,#1673,#1674,#1675));
#684=EDGE_LOOP('',(#1676,#1677,#1678,#1679));
#685=EDGE_LOOP('',(#1680));
#686=EDGE_LOOP('',(#1681));
#687=EDGE_LOOP('',(#1682));
#688=EDGE_LOOP('',(#1683));
#783=LINE('',#3448,#881);
#784=LINE('',#3454,#882);
#881=VECTOR('',#2867,5.);
#882=VECTOR('',#2874,10.);
#981=CIRCLE('',#2282,5.);
#982=CIRCLE('',#2283,5.);
#983=CIRCLE('',#2285,10.);
#984=CIRCLE('',#2286,10.);
#1108=VERTEX_POINT('',#3445);
#1109=VERTEX_POINT('',#3447);
#1110=VERTEX_POINT('',#3451);
#1111=VERTEX_POINT('',#3453);
#1298=EDGE_CURVE('',#1108,#1108,#981,.T.);
#1299=EDGE_CURVE('',#1108,#1109,#783,.T.);
#1300=EDGE_CURVE('',#1109,#1109,#982,.T.);
#1301=EDGE_CURVE('',#1110,#1110,#983,.T.);
#1302=EDGE_CURVE('',#1110,#1111,#784,.T.);
#1303=EDGE_CURVE('',#1111,#1111,#984,.T.);
#1672=ORIENTED_EDGE('',*,*,#1298,.F.);
#1673=ORIENTED_EDGE('',*,*,#1299,.T.);
#1674=ORIENTED_EDGE('',*,*,#1300,.T.);
#1675=ORIENTED_EDGE('',*,*,#1299,.F.);
#1676=ORIENTED_EDGE('',*,*,#1301,.F.);
#1677=ORIENTED_EDGE('',*,*,#1302,.T.);
#1678=ORIENTED_EDGE('',*,*,#1303,.T.);
#1679=ORIENTED_EDGE('',*,*,#1302,.F.);
#1680=ORIENTED_EDGE('',*,*,#1301,.T.);
#1681=ORIENTED_EDGE('',*,*,#1298,.T.);
#1682=ORIENTED_EDGE('',*,*,#1303,.F.);
#1683=ORIENTED_EDGE('',*,*,#1300,.F.);
#1753=CYLINDRICAL_SURFACE('',#2281,5.);
#1754=CYLINDRICAL_SURFACE('',#2284,10.);
#1858=ADVANCED_FACE('',(#526),#1753,.F.);
#1859=ADVANCED_FACE('',(#527),#1754,.T.);
#1860=ADVANCED_FACE('',(#528,#362),#419,.T.);
#1861=ADVANCED_FACE('',(#529,#363),#420,.F.);
#1883=CLOSED_SHELL('',(#1858,#1859,#1860,#1861));
#2280=AXIS2_PLACEMENT_3D('',#3443,#2861,#2862);
#2281=AXIS2_PLACEMENT_3D('',#3444,#2863,#2864);
#2282=AXIS2_PLACEMENT_3D('',#3446,#2865,#2866);
#2283=AXIS2_PLACEMENT_3D('',#3449,#2868,#2869);
#2284=AXIS2_PLACEMENT_3D('',#3450,#2870,#2871);
#2285=AXIS2_PLACEMENT_3D('',#3452,#2872,#2873);
#2286=AXIS2_PLACEMENT_3D('',#3455,#2875,#2876);
#2287=AXIS2_PLACEMENT_3D('',#3456,#2877,#2878);
#2288=AXIS2_PLACEMENT_3D('',#3457,#2879,#2880);
#2861=DIRECTION('axis',(0.,0.,1.));
#2862=DIRECTION('refdir',(1.,0.,0.));
#2863=DIRECTION('center_axis',(0.,0.,1.));
#2864=DIRECTION('ref_axis',(1.,0.,0.));
#2865=DIRECTION('center_axis',(0.,0.,-1.));
#2866=DIRECTION('ref_axis',(1.,0.,0.));
#2867=DIRECTION('',(0.,0.,-1.));
#2868=DIRECTION('center_axis',(0.,0.,-1.));
#2869=DIRECTION('ref_axis',(1.,0.,0.));
#2870=DIRECTION('center_axis',(0.,0.,1.));
#2871=DIRECTION('ref_axis',(1.,0.,0.));
#2872=DIRECTION('center_axis',(0.,0.,1.));
#2873=DIRECTION('ref_axis',(1.,0.,0.));
#2874=DIRECTION('',(0.,0.,-1.));
#2875=DIRECTION('center_axis',(0.,0.,1.));
#2876=DIRECTION('ref_axis',(1.,0.,0.));
#2877=DIRECTION('center_axis',(0.,0.,1.));
#2878=DIRECTION('ref_axis',(1.,0.,0.));
#2879=DIRECTION('center_axis',(0.,0.,1.));
#2880=DIRECTION('ref_axis',(1.,0.,0.));
#3443=CARTESIAN_POINT('',(0.,0.,0.));
#3444=CARTESIAN_POINT('Origin',(0.,0.,0.));
#3445=CARTESIAN_POINT('',(-5.,-6.12323399573677E-16,2.));
#3446=CARTESIAN_POINT('Origin',(0.,0.,2.));
#3447=CARTESIAN_POINT('',(-5.,-6.12323399573677E-16,0.));
#3448=CARTESIAN_POINT('',(-5.,-6.12323399573677E-16,0.));
#3449=CARTESIAN_POINT('Origin',(0.,0.,0.));
#3450=CARTESIAN_POINT('Origin',(0.,0.,0.));
#3451=CARTESIAN_POINT('',(-10.,-1.22464679914735E-15,2.));
#3452=CARTESIAN_POINT('Origin',(0.,0.,2.));
#3453=CARTESIAN_POINT('',(-10.,-1.22464679914735E-15,0.));
#3454=CARTESIAN_POINT('',(-10.,-1.22464679914735E-15,0.));
#3455=CARTESIAN_POINT('Origin',(0.,0.,0.));
#3456=CARTESIAN_POINT('Origin',(0.,0.,2.));
#3457=CARTESIAN_POINT('Origin',(0.,0.,0.));
#3560=UNCERTAINTY_MEASURE_WITH_UNIT(LENGTH_MEASURE(0.01),#3582,
'DISTANCE_ACCURACY_VALUE',
'Maximum model space distance between geometric entities at asserted c
onnectivities');
#3562=UNCERTAINTY_MEASURE_WITH_UNIT(LENGTH_MEASURE(0.01),#3582,
'DISTANCE_ACCURACY_VALUE',
'Maximum model space distance between geometric entities at asserted c
onnectivities');
#3579=(
GEOMETRIC_REPRESENTATION_CONTEXT(3)
GLOBAL_UNCERTAINTY_ASSIGNED_CONTEXT((#3560))
GLOBAL_UNIT_ASSIGNED_CONTEXT((#3582,#3584,#3585))
REPRESENTATION_CONTEXT('','3D')
);
#3581=(
GEOMETRIC_REPRESENTATION_CONTEXT(3)
GLOBAL_UNCERTAINTY_ASSIGNED_CONTEXT((#3562))
GLOBAL_UNIT_ASSIGNED_CONTEXT((#3582,#3584,#3585))
REPRESENTATION_CONTEXT('','3D')
);
#3582=(
LENGTH_UNIT()
NAMED_UNIT(*)
SI_UNIT(.MILLI.,.METRE.)
);
#3584=(
NAMED_UNIT(*)
PLANE_ANGLE_UNIT()
SI_UNIT($,.RADIAN.)
);
#3585=(
NAMED_UNIT(*)
SI_UNIT($,.STERADIAN.)
SOLID_ANGLE_UNIT()
);
#3602=SHAPE_DEFINITION_REPRESENTATION(#3620,#3697);
#3620=PRODUCT_DEFINITION_SHAPE('',$,#3716);
#3697=SHAPE_REPRESENTATION('',(#2280),#3579);
#3699=PRODUCT_DEFINITION_CONTEXT('part definition',#3755,'design');
#3716=PRODUCT_DEFINITION('Pivot washer','Pivot washer',#3734,#3699);
#3734=PRODUCT_DEFINITION_FORMATION('',$,#3773);
#3755=APPLICATION_CONTEXT(
'Core Data for Automotive Mechanical Design Process');
#3756=PRODUCT_CONTEXT('part definition',#3755,'mechanical');
#3773=PRODUCT('Pivot washer','Pivot washer',$,(#3756));
#3786=PRESENTATION_STYLE_ASSIGNMENT((#3799));
#3799=SURFACE_STYLE_USAGE(.BOTH.,#3812);
#3812=SURFACE_SIDE_STYLE('',(#3825));
#3825=SURFACE_STYLE_FILL_AREA(#3838);
#3838=FILL_AREA_STYLE('Washer light gray',(#3851));
#3851=FILL_AREA_STYLE_COLOUR('Washer light gray',#3864);
#3864=COLOUR_RGB('Washer light gray',0.725490196078431,0.752941176470588,
0.792156862745098);
ENDSEC;
END-ISO-10303-21;
